ISO-10303-21;
HEADER;
FILE_DESCRIPTION (('STEP AP214'),
    '1' );
FILE_NAME ( 'Side Bracket__PD14855.step', '2026-10-04T02:08:54', ( '' ), ( '' ), 'STEP AP214', 'Unspecified', '' );
FILE_SCHEMA (( 'AUTOMOTIVE_DESIGN' ));
ENDSEC;
DATA;
#95=DIRECTION ( 'NONE',  ( 1.000000000000000000, -0.000000000000000000, -1.144917494144692682E-16 ) ) ;
#106=EDGE_CURVE ( 'NONE', #13083, #24265, #27060, .T. ) ;
#186=ORIENTED_EDGE ( 'NONE', *, *, #26981, .F. ) ;
#371=DIRECTION ( 'NONE',  ( 0.000000000000000000, 0.000000000000000000, 1.000000000000000000 ) ) ;
#384=CARTESIAN_POINT ( 'NONE',  ( 0.6195511811023588500, -5.463695987328330208E-16, -1.186023622047243986 ) ) ;
#407=ORIENTED_EDGE ( 'NONE', *, *, #24032, .F. ) ;
#486=LINE ( 'NONE', #44113, #7940 ) ;
#496=CARTESIAN_POINT ( 'NONE',  ( 0.6195511811023624027, 0.9842519685039370358, -0.8759842519685050455 ) ) ;
#549=CARTESIAN_POINT ( 'NONE',  ( 0.6195511811023604043, 0.4133858267716528090, 0.9891732283464566011 ) ) ;
#554=EDGE_CURVE ( 'NONE', #37817, #25198, #47100, .T. ) ;
#561=DIRECTION ( 'NONE',  ( 1.144917494144692682E-16, -3.972230510298676574E-31, 1.000000000000000000 ) ) ;
#569=ORIENTED_EDGE ( 'NONE', *, *, #21974, .T. ) ;
#709=CIRCLE ( 'NONE', #12248, 0.1968503937007874127 ) ;
#716=DIRECTION ( 'NONE',  ( 1.000000000000000000, -3.469446951953614978E-15, -1.144917494144692929E-16 ) ) ;
#786=EDGE_CURVE ( 'NONE', #42479, #21227, #41230, .T. ) ;
#795=LINE ( 'NONE', #37964, #37288 ) ;
#822=ORIENTED_EDGE ( 'NONE', *, *, #16650, .T. ) ;
#865=CARTESIAN_POINT ( 'NONE',  ( -0.1377952755905511861, 0.1574803149606320007, -0.8070866141732283561 ) ) ;
#876=VECTOR ( 'NONE', #10922, 39.37007874015748143 ) ;
#894=VERTEX_POINT ( 'NONE', #40177 ) ;
#1010=ORIENTED_EDGE ( 'NONE', *, *, #106, .T. ) ;
#1079=DIRECTION ( 'NONE',  ( 3.469446951953613794E-15, 1.000000000000000000, 1.020425574103997713E-16 ) ) ;
#1110=DIRECTION ( 'NONE',  ( -1.144917494144692682E-16, -2.347476851301873745E-33, -1.000000000000000000 ) ) ;
#1171=ORIENTED_EDGE ( 'NONE', *, *, #34714, .F. ) ;
#1261=ORIENTED_EDGE ( 'NONE', *, *, #13253, .T. ) ;
#1302=ORIENTED_EDGE ( 'NONE', *, *, #20125, .F. ) ;
#1317=CARTESIAN_POINT ( 'NONE',  ( 0.4620708661417356478, 0.9842519685039370358, -0.8759842519685050455 ) ) ;
#1340=ADVANCED_FACE ( 'NONE', ( #5541, #31206 ), #42645, .T. ) ;
#1367=CARTESIAN_POINT ( 'NONE',  ( -0.1377952755905511861, 0.1574803149606320007, -0.8070866141732283561 ) ) ;
#1466=ORIENTED_EDGE ( 'NONE', *, *, #25772, .F. ) ;
#1513=DIRECTION ( 'NONE',  ( -1.144917494144692682E-16, 5.091027988365947196E-31, -1.000000000000000000 ) ) ;
#1596=CARTESIAN_POINT ( 'NONE',  ( -0.1377952755905511861, 0.1564960629921283985, -0.8070866141732283561 ) ) ;
#1600=CIRCLE ( 'NONE', #42131, 0.1968503937007874127 ) ;
#1676=AXIS2_PLACEMENT_3D ( 'NONE', #22841, #34127, #40789 ) ;
#1701=AXIS2_PLACEMENT_3D ( 'NONE', #24854, #9540, #24162 ) ;
#1702=AXIS2_PLACEMENT_3D ( 'NONE', #14220, #14450, #28368 ) ;
#1932=DIRECTION ( 'NONE',  ( -1.000000000000000000, 3.469446951953613794E-15, 1.144917494144692682E-16 ) ) ;
#1966=VERTEX_POINT ( 'NONE', #18807 ) ;
#2086=CARTESIAN_POINT ( 'NONE',  ( 0.6195511811023610704, 0.6102362204724403050, 0.5167322834645649010 ) ) ;
#2107=CARTESIAN_POINT ( 'NONE',  ( 0.4620708661417344820, 0.6102362204724408601, 0.5854071585544579071 ) ) ;
#2262=VERTEX_POINT ( 'NONE', #20698 ) ;
#2306=ORIENTED_EDGE ( 'NONE', *, *, #31742, .T. ) ;
#2315=EDGE_CURVE ( 'NONE', #3713, #30859, #28291, .T. ) ;
#2533=VERTEX_POINT ( 'NONE', #45242 ) ;
#2563=ORIENTED_EDGE ( 'NONE', *, *, #13616, .T. ) ;
#2807=ORIENTED_EDGE ( 'NONE', *, *, #4460, .F. ) ;
#2866=ORIENTED_EDGE ( 'NONE', *, *, #24415, .F. ) ;
#2873=LINE ( 'NONE', #39303, #35054 ) ;
#2885=VECTOR ( 'NONE', #9072, 39.37007874015748143 ) ;
#2891=LINE ( 'NONE', #17768, #16244 ) ;
#3083=VERTEX_POINT ( 'NONE', #34152 ) ;
#3097=DIRECTION ( 'NONE',  ( -1.144917494144692682E-16, 3.972230510298674823E-31, -1.000000000000000000 ) ) ;
#3179=AXIS2_PLACEMENT_3D ( 'NONE', #18558, #11154, #32969 ) ;
#3195=EDGE_CURVE ( 'NONE', #22011, #37817, #22200, .T. ) ;
#3234=FACE_OUTER_BOUND ( 'NONE', #27702, .T. ) ;
#3289=DIRECTION ( 'NONE',  ( 0.000000000000000000, 0.000000000000000000, 1.000000000000000000 ) ) ;
#3292=CARTESIAN_POINT ( 'NONE',  ( -0.2362204724409469325, 8.195543980992859667E-16, 0.9891732283464568232 ) ) ;
#3325=DIRECTION ( 'NONE',  ( 0.000000000000000000, 0.000000000000000000, 1.000000000000000000 ) ) ;
#3336=VERTEX_POINT ( 'NONE', #4931 ) ;
#3364=ORIENTED_EDGE ( 'NONE', *, *, #37271, .F. ) ;
#3376=EDGE_CURVE ( 'NONE', #7349, #3083, #10152, .T. ) ;
#3381=VERTEX_POINT ( 'NONE', #37531 ) ;
#3457=AXIS2_PLACEMENT_3D ( 'NONE', #1367, #16022, #31816 ) ;
#3491=CARTESIAN_POINT ( 'NONE',  ( 0.4620708661417345930, 0.6529540528279709211, 0.4629603087243970849 ) ) ;
#3521=ADVANCED_FACE ( 'NONE', ( #23159 ), #45645, .T. ) ;
#3583=EDGE_CURVE ( 'NONE', #46340, #15018, #34907, .T. ) ;
#3682=ORIENTED_EDGE ( 'NONE', *, *, #15135, .T. ) ;
#3691=APPLICATION_CONTEXT ( 'automotive_design' ) ;
#3713=VERTEX_POINT ( 'NONE', #2107 ) ;
#3871=( LENGTH_UNIT ( ) NAMED_UNIT ( * ) SI_UNIT ( $, .METRE. ) ) ;
#3903=EDGE_CURVE ( 'NONE', #21477, #40961, #16322, .T. ) ;
#3975=CARTESIAN_POINT ( 'NONE',  ( 0.6195511811023624027, 0.9842519685039370358, -0.5511811023622036343 ) ) ;
#3997=CARTESIAN_POINT ( 'NONE',  ( 0.6195511811023612925, 0.6529540528279703659, 0.4629603087243970849 ) ) ;
#4000=VERTEX_POINT ( 'NONE', #1317 ) ;
#4102=ADVANCED_FACE ( 'NONE', ( #42216 ), #15498, .T. ) ;
#4136=AXIS2_PLACEMENT_3D ( 'NONE', #27125, #30952, #45286 ) ;
#4137=VERTEX_POINT ( 'NONE', #41315 ) ;
#4213=CARTESIAN_POINT ( 'NONE',  ( -0.4330708661417337901, 0.1574803149606330277, 0.9891732283464568232 ) ) ;
#4302=ADVANCED_FACE ( 'NONE', ( #20891 ), #35532, .F. ) ;
#4394=ORIENTED_EDGE ( 'NONE', *, *, #25772, .T. ) ;
#4417=EDGE_CURVE ( 'NONE', #4137, #38595, #486, .T. ) ;
#4450=DIRECTION ( 'NONE',  ( -1.000000000000000000, 3.469446951953613794E-15, 1.144917494144692682E-16 ) ) ;
#4460=EDGE_CURVE ( 'NONE', #894, #45730, #7163, .T. ) ;
#4524=EDGE_CURVE ( 'NONE', #39582, #3381, #29455, .T. ) ;
#4586=DIRECTION ( 'NONE',  ( -3.469446951953614189E-15, -1.000000000000000000, -1.118797478067273468E-31 ) ) ;
#4642=ORIENTED_EDGE ( 'NONE', *, *, #11875, .T. ) ;
#4656=ORIENTED_EDGE ( 'NONE', *, *, #24415, .T. ) ;
#4768=ORIENTED_EDGE ( 'NONE', *, *, #26760, .F. ) ;
#4931=CARTESIAN_POINT ( 'NONE',  ( -0.2362204724409471546, 2.422684756221294029E-15, -1.186023622047243986 ) ) ;
#4959=DIRECTION ( 'NONE',  ( -0.000000000000000000, 1.000000000000000000, -3.995705278811693553E-31 ) ) ;
#4968=CARTESIAN_POINT ( 'NONE',  ( -0.2362204724409471546, 8.195543980992867555E-16, -0.9891732283464564901 ) ) ;
#5195=AXIS2_PLACEMENT_3D ( 'NONE', #25872, #29283, #44287 ) ;
#5212=FACE_OUTER_BOUND ( 'NONE', #36520, .T. ) ;
#5371=ORIENTED_EDGE ( 'NONE', *, *, #30888, .T. ) ;
#5412=DIRECTION ( 'NONE',  ( 0.000000000000000000, 0.000000000000000000, 1.000000000000000000 ) ) ;
#5439=DIRECTION ( 'NONE',  ( 0.000000000000000000, 0.000000000000000000, -1.000000000000000000 ) ) ;
#5541=FACE_BOUND ( 'NONE', #38113, .T. ) ;
#5613=LINE ( 'NONE', #26736, #46853 ) ;
#5620=ORIENTED_EDGE ( 'NONE', *, *, #11122, .T. ) ;
#5666=DIMENSIONAL_EXPONENTS ( 1.000000000000000000, 0.000000000000000000, 0.000000000000000000, 0.000000000000000000, 0.000000000000000000, 0.000000000000000000, 0.000000000000000000 ) ;
#5782=VECTOR ( 'NONE', #44968, 39.37007874015748143 ) ;
#5872=VERTEX_POINT ( 'NONE', #28514 ) ;
#5919=ORIENTED_EDGE ( 'NONE', *, *, #4524, .T. ) ;
#5989=CARTESIAN_POINT ( 'NONE',  ( 0.4620708661417351482, 0.8070866141732281340, 0.5854071585544579071 ) ) ;
#6053=VECTOR ( 'NONE', #23843, 39.37007874015748143 ) ;
#6225=CARTESIAN_POINT ( 'NONE',  ( 0.4620708661417355922, 0.9842519685039372579, -1.186023622047244430 ) ) ;
#6302=DIRECTION ( 'NONE',  ( 1.000000000000000000, -3.469446951953614583E-15, -1.151683635503274272E-16 ) ) ;
#6320=EDGE_CURVE ( 'NONE', #9932, #2533, #25713, .T. ) ;
#6321=ORIENTED_EDGE ( 'NONE', *, *, #2315, .F. ) ;
#6359=AXIS2_PLACEMENT_3D ( 'NONE', #26493, #37250, #8014 ) ;
#6481=ADVANCED_FACE ( 'NONE', ( #41541 ), #8744, .F. ) ;
#6505=DIRECTION ( 'NONE',  ( 0.000000000000000000, 0.000000000000000000, -1.000000000000000000 ) ) ;
#6512=ADVANCED_FACE ( 'NONE', ( #45397 ), #31983, .T. ) ;
#6569=CARTESIAN_POINT ( 'NONE',  ( 0.6195511811023612925, 0.6102362204724401940, 0.9891732283464566011 ) ) ;
#6591=EDGE_CURVE ( 'NONE', #2533, #27462, #26573, .T. ) ;
#6646=DIRECTION ( 'NONE',  ( 1.000000000000000000, -3.469446951953614583E-15, 0.000000000000000000 ) ) ;
#6733=ORIENTED_EDGE ( 'NONE', *, *, #4460, .T. ) ;
#6749=EDGE_CURVE ( 'NONE', #4137, #28233, #13821, .T. ) ;
#6828=CARTESIAN_POINT ( 'NONE',  ( 0.6195511811023624027, 0.9842519685039370358, -0.7135826771653542844 ) ) ;
#6832=DIRECTION ( 'NONE',  ( -3.364312195833787750E-15, -1.000000000000000000, 0.000000000000000000 ) ) ;
#6860=VERTEX_POINT ( 'NONE', #32534 ) ;
#6935=CIRCLE ( 'NONE', #40614, 0.4724409448818900348 ) ;
#7035=ORIENTED_EDGE ( 'NONE', *, *, #37774, .F. ) ;
#7064=LINE ( 'NONE', #32735, #876 ) ;
#7163=CIRCLE ( 'NONE', #20939, 0.1968503937007874405 ) ;
#7172=LINE ( 'NONE', #47431, #44649 ) ;
#7216=DIRECTION ( 'NONE',  ( -1.000000000000000000, 0.000000000000000000, 0.000000000000000000 ) ) ;
#7302=CARTESIAN_POINT ( 'NONE',  ( -0.1377952755905511584, 0.1564960629921283985, 0.7066929133858274037 ) ) ;
#7324=DIRECTION ( 'NONE',  ( -3.469446951953614978E-15, -1.000000000000000000, 3.995705278811693553E-31 ) ) ;
#7349=VERTEX_POINT ( 'NONE', #6569 ) ;
#7414=CARTESIAN_POINT ( 'NONE',  ( 0.4620708661417356478, 0.9842519685039370358, -0.7135826771653542844 ) ) ;
#7442=ORIENTED_EDGE ( 'NONE', *, *, #3583, .T. ) ;
#7580=LINE ( 'NONE', #384, #14108 ) ;
#7770=CARTESIAN_POINT ( 'NONE',  ( 0.4620708661417344820, 0.6102362204724408601, 0.5854071585544579071 ) ) ;
#7806=ORIENTED_EDGE ( 'NONE', *, *, #13961, .F. ) ;
#7895=FACE_BOUND ( 'NONE', #14239, .T. ) ;
#7940=VECTOR ( 'NONE', #716, 39.37007874015748143 ) ;
#8014=DIRECTION ( 'NONE',  ( -3.469446951953612217E-15, -1.000000000000000000, 0.000000000000000000 ) ) ;
#8092=AXIS2_PLACEMENT_3D ( 'NONE', #865, #15769, #33278 ) ;
#8213=AXIS2_PLACEMENT_3D ( 'NONE', #40116, #95, #18332 ) ;
#8291=CARTESIAN_POINT ( 'NONE',  ( 0.4620708661417338714, 0.4133858267716533641, 0.9891732283464566011 ) ) ;
#8392=ORIENTED_EDGE ( 'NONE', *, *, #22082, .T. ) ;
#8398=EDGE_CURVE ( 'NONE', #8725, #46340, #21021, .T. ) ;
#8492=DIRECTION ( 'NONE',  ( 2.055777091826793380E-15, 0.6220299971367094782, -0.7829934116339072325 ) ) ;
#8590=DIRECTION ( 'NONE',  ( -1.000000000000000000, 3.469446951953613794E-15, 1.144917494144692682E-16 ) ) ;
#8593=VECTOR ( 'NONE', #44466, 39.37007874015748143 ) ;
#8630=ORIENTED_EDGE ( 'NONE', *, *, #13616, .F. ) ;
#8725=VERTEX_POINT ( 'NONE', #13196 ) ;
#8744=CYLINDRICAL_SURFACE ( 'NONE', #11926, 0.1968503937007874405 ) ;
#8777=VERTEX_POINT ( 'NONE', #34770 ) ;
#8819=DIRECTION ( 'NONE',  ( -3.469446951953612217E-15, -1.000000000000000000, 0.000000000000000000 ) ) ;
#8874=CIRCLE ( 'NONE', #28735, 0.1003937007874010356 ) ;
#9072=DIRECTION ( 'NONE',  ( 1.000000000000000000, -0.000000000000000000, -1.144917494144692682E-16 ) ) ;
#9219=DIRECTION ( 'NONE',  ( -1.151683635503274519E-16, -0.000000000000000000, -1.000000000000000000 ) ) ;
#9286=EDGE_LOOP ( 'NONE', ( #33720, #2563, #822, #27835 ) ) ;
#9295=ORIENTED_EDGE ( 'NONE', *, *, #6320, .T. ) ;
#9319=FACE_BOUND ( 'NONE', #13609, .T. ) ;
#9376=EDGE_CURVE ( 'NONE', #27462, #21477, #41957, .T. ) ;
#9466=CARTESIAN_POINT ( 'NONE',  ( 0.4620708661417330387, 0.1864803149606299171, 1.186023622047243986 ) ) ;
#9540=DIRECTION ( 'NONE',  ( 0.000000000000000000, 1.000000000000000000, 0.000000000000000000 ) ) ;
#9627=DIRECTION ( 'NONE',  ( -3.469446951953613794E-15, -1.000000000000000000, 0.000000000000000000 ) ) ;
#9857=DIRECTION ( 'NONE',  ( -1.000000000000000000, 3.469446951953613794E-15, 1.144917494144692682E-16 ) ) ;
#9924=FACE_OUTER_BOUND ( 'NONE', #14575, .T. ) ;
#9932=VERTEX_POINT ( 'NONE', #44072 ) ;
#9967=EDGE_LOOP ( 'NONE', ( #29933, #39210, #38756, #569 ) ) ;
#10043=CIRCLE ( 'NONE', #12356, 0.1003937007874010356 ) ;
#10152=CIRCLE ( 'NONE', #11696, 0.1968503937007874127 ) ;
#10209=VECTOR ( 'NONE', #4959, 39.37007874015748143 ) ;
#10211=EDGE_LOOP ( 'NONE', ( #4768, #46041, #20532, #19612 ) ) ;
#10235=ORIENTED_EDGE ( 'NONE', *, *, #11655, .T. ) ;
#10263=CARTESIAN_POINT ( 'NONE',  ( -0.1377952755905511861, 0.1564960629921283985, -0.8070866141732283561 ) ) ;
#10264=FACE_OUTER_BOUND ( 'NONE', #15590, .T. ) ;
#10277=ORIENTED_EDGE ( 'NONE', *, *, #21912, .T. ) ;
#10453=CYLINDRICAL_SURFACE ( 'NONE', #40226, 0.1624015748031507056 ) ;
#10671=AXIS2_PLACEMENT_3D ( 'NONE', #20154, #9857, #24467 ) ;
#10705=ORIENTED_EDGE ( 'NONE', *, *, #9376, .T. ) ;
#10755=DIRECTION ( 'NONE',  ( -1.020425574104001164E-16, 1.020425574104001164E-16, -1.000000000000000000 ) ) ;
#10762=ADVANCED_FACE ( 'NONE', ( #40578 ), #39639, .T. ) ;
#10785=EDGE_CURVE ( 'NONE', #21227, #42479, #25852, .T. ) ;
#10821=CARTESIAN_POINT ( 'NONE',  ( -0.4330708661417340677, 0.1574803149606330277, -1.186023622047243986 ) ) ;
#10831=CARTESIAN_POINT ( 'NONE',  ( 0.4330708661417329020, 0.1864803149606300281, -1.186023622047243986 ) ) ;
#10835=DIRECTION ( 'NONE',  ( 1.000000000000000000, 0.000000000000000000, 0.000000000000000000 ) ) ;
#10886=EDGE_LOOP ( 'NONE', ( #14465, #46016, #10705, #35219 ) ) ;
#10903=EDGE_CURVE ( 'NONE', #28143, #6860, #795, .T. ) ;
#10922=DIRECTION ( 'NONE',  ( -3.469446951953614583E-15, -1.000000000000000000, 0.000000000000000000 ) ) ;
#10982=DIRECTION ( 'NONE',  ( 0.000000000000000000, 1.000000000000000000, 0.000000000000000000 ) ) ;
#10986=DIRECTION ( 'NONE',  ( 0.000000000000000000, 0.000000000000000000, -1.000000000000000000 ) ) ;
#11025=EDGE_LOOP ( 'NONE', ( #29013, #14993, #45918, #16432 ) ) ;
#11031=LINE ( 'NONE', #22258, #33863 ) ;
#11037=CARTESIAN_POINT ( 'NONE',  ( -0.4330708661417337901, 0.1574803149606330277, 0.9891732283464566011 ) ) ;
#11050=ORIENTED_EDGE ( 'NONE', *, *, #3903, .F. ) ;
#11120=ORIENTED_EDGE ( 'NONE', *, *, #13125, .T. ) ;
#11122=EDGE_CURVE ( 'NONE', #30632, #27780, #41769, .T. ) ;
#11154=DIRECTION ( 'NONE',  ( -0.000000000000000000, 1.000000000000000000, -3.995705278811693553E-31 ) ) ;
#11215=DIRECTION ( 'NONE',  ( -1.000000000000000000, 3.469446951953613794E-15, 1.144917494144692682E-16 ) ) ;
#11307=LENGTH_MEASURE_WITH_UNIT ( LENGTH_MEASURE( 0.02539999999999999897 ), #25460 ) ;
#11362=FACE_OUTER_BOUND ( 'NONE', #10886, .T. ) ;
#11400=ADVANCED_FACE ( 'NONE', ( #9924 ), #24531, .F. ) ;
#11411=CARTESIAN_POINT ( 'NONE',  ( -0.1377952755905511861, -1.331775896911328393E-15, 0.8070866141732283561 ) ) ;
#11415=CYLINDRICAL_SURFACE ( 'NONE', #42497, 0.1003937007874010356 ) ;
#11507=VECTOR ( 'NONE', #4450, 39.37007874015748143 ) ;
#11578=CARTESIAN_POINT ( 'NONE',  ( -0.2362204724409469325, 2.422684756221293634E-15, 0.9891732283464568232 ) ) ;
#11655=EDGE_CURVE ( 'NONE', #24265, #6860, #2873, .T. ) ;
#11657=DIRECTION ( 'NONE',  ( 0.000000000000000000, 0.000000000000000000, 1.000000000000000000 ) ) ;
#11689=DIRECTION ( 'NONE',  ( 1.000000000000000000, -0.000000000000000000, -1.144917494144692682E-16 ) ) ;
#11696=AXIS2_PLACEMENT_3D ( 'NONE', #30608, #30156, #23867 ) ;
#11875=EDGE_CURVE ( 'NONE', #8777, #8725, #43611, .T. ) ;
#11926=AXIS2_PLACEMENT_3D ( 'NONE', #27470, #42021, #20235 ) ;
#12108=ORIENTED_EDGE ( 'NONE', *, *, #8398, .F. ) ;
#12248=AXIS2_PLACEMENT_3D ( 'NONE', #11578, #4586, #40771 ) ;
#12299=AXIS2_PLACEMENT_3D ( 'NONE', #22088, #37590, #25475 ) ;
#12348=AXIS2_PLACEMENT_3D ( 'NONE', #19797, #38251, #5412 ) ;
#12356=AXIS2_PLACEMENT_3D ( 'NONE', #14379, #32844, #47439 ) ;
#12522=CARTESIAN_POINT ( 'NONE',  ( 0.4620708661417338714, 0.4133858267716533641, 1.186023622047243986 ) ) ;
#12664=DIRECTION ( 'NONE',  ( -1.000000000000000000, 3.469446951953613794E-15, 1.144917494144692682E-16 ) ) ;
#12695=CARTESIAN_POINT ( 'NONE',  ( 0.6195511811023624027, 0.9842519685039370358, -0.5511811023622036343 ) ) ;
#12697=DIRECTION ( 'NONE',  ( -1.000000000000000000, 3.469446951953614189E-15, 1.144917494144692682E-16 ) ) ;
#12777=CARTESIAN_POINT ( 'NONE',  ( -0.1377952755905511861, 0.1564960629921283985, 0.9074803149606294195 ) ) ;
#12793=VECTOR ( 'NONE', #15903, 39.37007874015748854 ) ;
#12862=CARTESIAN_POINT ( 'NONE',  ( 0.4330708661417295158, 0.1864803149606300281, -1.186023622047243986 ) ) ;
#12884=APPLICATION_CONTEXT ( 'automotive_design' ) ;
#12942=ORIENTED_EDGE ( 'NONE', *, *, #10903, .T. ) ;
#12996=ORIENTED_EDGE ( 'NONE', *, *, #37325, .F. ) ;
#13073=ORIENTED_EDGE ( 'NONE', *, *, #34714, .T. ) ;
#13083=VERTEX_POINT ( 'NONE', #18177 ) ;
#13125=EDGE_CURVE ( 'NONE', #5872, #30632, #18292, .T. ) ;
#13165=DIRECTION ( 'NONE',  ( -3.469446951953612217E-15, -1.000000000000000000, 0.000000000000000000 ) ) ;
#13196=CARTESIAN_POINT ( 'NONE',  ( 0.4330708661417325689, 0.1574803149606300301, -1.186023622047243986 ) ) ;
#13253=EDGE_CURVE ( 'NONE', #3083, #22876, #34450, .T. ) ;
#13265=CLOSED_SHELL ( 'NONE', ( #21647, #46296, #4302, #20406, #44898, #22446, #4102, #10762, #29809, #17996, #25341, #41850, #34271, #1340, #11400, #38627, #46135, #38942, #45916, #46989, #30484, #3521, #6512, #33745, #26269, #6481 ) ) ;
#13499=DIRECTION ( 'NONE',  ( -0.000000000000000000, 1.000000000000000000, -3.995705278811693553E-31 ) ) ;
#13555=FACE_OUTER_BOUND ( 'NONE', #9286, .T. ) ;
#13609=EDGE_LOOP ( 'NONE', ( #27314, #14768 ) ) ;
#13616=EDGE_CURVE ( 'NONE', #9932, #15531, #21956, .T. ) ;
#13821=LINE ( 'NONE', #25080, #21094 ) ;
#13961=EDGE_CURVE ( 'NONE', #1966, #22011, #27933, .T. ) ;
#13989=EDGE_LOOP ( 'NONE', ( #37680, #15341, #407, #37920, #30565, #1261, #25522, #22502 ) ) ;
#14108=VECTOR ( 'NONE', #22193, 39.37007874015748143 ) ;
#14175=AXIS2_PLACEMENT_3D ( 'NONE', #10831, #25194, #7216 ) ;
#14184=ORIENTED_EDGE ( 'NONE', *, *, #4524, .F. ) ;
#14220=CARTESIAN_POINT ( 'NONE',  ( -0.4330708661417340677, 0.1574803149606330277, -1.186023622047243986 ) ) ;
#14236=ORIENTED_EDGE ( 'NONE', *, *, #18029, .T. ) ;
#14239=EDGE_LOOP ( 'NONE', ( #34849, #9295 ) ) ;
#14268=CARTESIAN_POINT ( 'NONE',  ( 0.6195511811023597382, 0.1864803149606293620, 1.186023622047243986 ) ) ;
#14337=CARTESIAN_POINT ( 'NONE',  ( 0.6195511811023621807, 0.9842519685039367028, -1.186023622047244430 ) ) ;
#14353=EDGE_CURVE ( 'NONE', #2262, #17766, #43687, .T. ) ;
#14379=CARTESIAN_POINT ( 'NONE',  ( -0.1377952755905511861, 0.1564960629921283985, 0.8070866141732283561 ) ) ;
#14387=CARTESIAN_POINT ( 'NONE',  ( 0.4330708661417331795, 0.1864803149606300281, 1.186023622047243986 ) ) ;
#14450=DIRECTION ( 'NONE',  ( -3.469446951953614978E-15, -1.000000000000000000, 3.995705278811693553E-31 ) ) ;
#14465=ORIENTED_EDGE ( 'NONE', *, *, #40238, .F. ) ;
#14524=CARTESIAN_POINT ( 'NONE',  ( -0.4330708661417340677, 0.1574803149606330277, -1.186023622047243986 ) ) ;
#14567=CARTESIAN_POINT ( 'NONE',  ( 0.4620708661417345375, 0.6102362204724407491, 1.186023622047243986 ) ) ;
#14575=EDGE_LOOP ( 'NONE', ( #36427, #10277, #41225, #27340 ) ) ;
#14582=CARTESIAN_POINT ( 'NONE',  ( 0.6195511811023621807, 0.9842519685039367028, -1.186023622047244430 ) ) ;
#14611=AXIS2_PLACEMENT_3D ( 'NONE', #7414, #22920, #34424 ) ;
#14643=ORIENTED_EDGE ( 'NONE', *, *, #6749, .F. ) ;
#14733=DIRECTION ( 'NONE',  ( 8.659560562358538199E-17, 0.7071067811862530306, -0.7071067811868418929 ) ) ;
#14745=ORIENTED_EDGE ( 'NONE', *, *, #31742, .F. ) ;
#14760=ORIENTED_EDGE ( 'NONE', *, *, #24214, .F. ) ;
#14768=ORIENTED_EDGE ( 'NONE', *, *, #786, .F. ) ;
#14843=DIRECTION ( 'NONE',  ( 3.469446951953615767E-15, 1.000000000000000000, 0.000000000000000000 ) ) ;
#14855=PRODUCT_DEFINITION ( 'UNKNOWN', '', #32422, #22108 ) ;
#14881=CARTESIAN_POINT ( 'NONE',  ( -0.1377952755905511861, 0.1574803149606320007, 0.9084645669291337988 ) ) ;
#14963=CARTESIAN_POINT ( 'NONE',  ( -0.1377952755905511861, 0.1564960629921283985, 0.8070866141732283561 ) ) ;
#14993=ORIENTED_EDGE ( 'NONE', *, *, #26981, .T. ) ;
#15018=VERTEX_POINT ( 'NONE', #9466 ) ;
#15081=ORIENTED_EDGE ( 'NONE', *, *, #38885, .F. ) ;
#15097=CARTESIAN_POINT ( 'NONE',  ( -0.2362204724409465995, 0.1574803149606323616, -0.9891732283464564901 ) ) ;
#15135=EDGE_CURVE ( 'NONE', #28233, #22011, #709, .T. ) ;
#15250=CARTESIAN_POINT ( 'NONE',  ( -0.1377952755905511584, 0.1574803149606320007, 0.7066929133858274037 ) ) ;
#15280=CYLINDRICAL_SURFACE ( 'NONE', #8092, 0.1003937007874010356 ) ;
#15341=ORIENTED_EDGE ( 'NONE', *, *, #6749, .T. ) ;
#15365=EDGE_LOOP ( 'NONE', ( #41480, #13073 ) ) ;
#15375=DIRECTION ( 'NONE',  ( -3.469446951953613794E-15, -1.000000000000000000, 0.000000000000000000 ) ) ;
#15376=( CONVERSION_BASED_UNIT ( 'INCH', #11307 ) LENGTH_UNIT ( ) NAMED_UNIT ( #5666 ) ) ;
#15498=PLANE ( 'NONE',  #34687 ) ;
#15521=VECTOR ( 'NONE', #1932, 39.37007874015748143 ) ;
#15531=VERTEX_POINT ( 'NONE', #24706 ) ;
#15589=ORIENTED_EDGE ( 'NONE', *, *, #19950, .T. ) ;
#15590=EDGE_LOOP ( 'NONE', ( #21468, #14643, #35548, #36815 ) ) ;
#15619=CARTESIAN_POINT ( 'NONE',  ( 0.6195511811023619586, 0.8070866141732275789, 0.5854071585544579071 ) ) ;
#15681=CIRCLE ( 'NONE', #21789, 0.02900000000000001882 ) ;
#15726=ORIENTED_EDGE ( 'NONE', *, *, #41511, .F. ) ;
#15736=CIRCLE ( 'NONE', #3457, 0.1013779527559055538 ) ;
#15769=DIRECTION ( 'NONE',  ( -0.000000000000000000, 1.000000000000000000, -3.995705278811693553E-31 ) ) ;
#15876=EDGE_LOOP ( 'NONE', ( #7806, #27096, #1466, #41116, #46969, #3682 ) ) ;
#15903=DIRECTION ( 'NONE',  ( 0.000000000000000000, 0.7071067811862530306, 0.7071067811868418929 ) ) ;
#16008=ORIENTED_EDGE ( 'NONE', *, *, #20066, .T. ) ;
#16022=DIRECTION ( 'NONE',  ( -3.469446951953614978E-15, -1.000000000000000000, 3.995705278811693553E-31 ) ) ;
#16043=VECTOR ( 'NONE', #39615, 39.37007874015748143 ) ;
#16244=VECTOR ( 'NONE', #36470, 39.37007874015748143 ) ;
#16248=ORIENTED_EDGE ( 'NONE', *, *, #38544, .T. ) ;
#16276=ORIENTED_EDGE ( 'NONE', *, *, #27598, .T. ) ;
#16322=CIRCLE ( 'NONE', #20130, 0.1013779527559055538 ) ;
#16385=DIMENSIONAL_EXPONENTS ( 1.000000000000000000, 0.000000000000000000, 0.000000000000000000, 0.000000000000000000, 0.000000000000000000, 0.000000000000000000, 0.000000000000000000 ) ;
#16432=ORIENTED_EDGE ( 'NONE', *, *, #33471, .F. ) ;
#16471=ORIENTED_EDGE ( 'NONE', *, *, #13125, .F. ) ;
#16649=ORIENTED_EDGE ( 'NONE', *, *, #42061, .F. ) ;
#16650=EDGE_CURVE ( 'NONE', #15531, #27462, #29185, .T. ) ;
#16738=LINE ( 'NONE', #12695, #2885 ) ;
#16924=CARTESIAN_POINT ( 'NONE',  ( -0.1377952755905511584, 0.1564960629921283985, -0.9074803149606294195 ) ) ;
#16934=EDGE_LOOP ( 'NONE', ( #2866, #26929, #20964, #11120 ) ) ;
#17026=FILL_AREA_STYLE_COLOUR ( '', #46055 ) ;
#17147=ORIENTED_EDGE ( 'NONE', *, *, #10785, .T. ) ;
#17311=CARTESIAN_POINT ( 'NONE',  ( 0.4620708661417369245, 1.354170115732555191, -0.4197102375732078561 ) ) ;
#17406=ORIENTED_EDGE ( 'NONE', *, *, #3376, .F. ) ;
#17559=FACE_BOUND ( 'NONE', #37076, .T. ) ;
#17604=DIRECTION ( 'NONE',  ( -1.020425574104001164E-16, 1.020425574104001164E-16, -1.000000000000000000 ) ) ;
#17669=CARTESIAN_POINT ( 'NONE',  ( -0.1377952755905511861, 0.1574803149606320007, 0.8070866141732283561 ) ) ;
#17674=LINE ( 'NONE', #14567, #33737 ) ;
#17720=CONICAL_SURFACE ( 'NONE', #20050, 0.1003937007874010356, 0.7853981633978647237 ) ;
#17723=DIRECTION ( 'NONE',  ( -1.000000000000000000, 0.000000000000000000, 1.144917494144692682E-16 ) ) ;
#17728=CARTESIAN_POINT ( 'NONE',  ( 0.6195511811023610704, 0.6102362204724403050, 0.5167322834645649010 ) ) ;
#17766=VERTEX_POINT ( 'NONE', #31187 ) ;
#17768=CARTESIAN_POINT ( 'NONE',  ( 0.6195511811023612925, 0.6102362204724401940, 0.9891732283464566011 ) ) ;
#17841=FACE_OUTER_BOUND ( 'NONE', #25390, .T. ) ;
#17996=ADVANCED_FACE ( 'NONE', ( #25644 ), #28539, .T. ) ;
#18029=EDGE_CURVE ( 'NONE', #27462, #15531, #10043, .T. ) ;
#18102=CARTESIAN_POINT ( 'NONE',  ( -0.1377952755905511861, 0.1564960629921283985, -0.8070866141732283561 ) ) ;
#18155=DIRECTION ( 'NONE',  ( -3.469446951953614583E-15, -1.000000000000000000, -1.751623080406021339E-46 ) ) ;
#18177=CARTESIAN_POINT ( 'NONE',  ( 0.6195511811023636239, 1.354170115732554747, -0.4197102375732078561 ) ) ;
#18292=CIRCLE ( 'NONE', #26718, 0.1003937007874010356 ) ;
#18300=EDGE_CURVE ( 'NONE', #41049, #46340, #20551, .T. ) ;
#18332=DIRECTION ( 'NONE',  ( 0.000000000000000000, 0.000000000000000000, -1.000000000000000000 ) ) ;
#18342=CARTESIAN_POINT ( 'NONE',  ( -0.1377952755905511861, 0.1574803149606320007, -0.8070866141732283561 ) ) ;
#18367=ORIENTED_EDGE ( 'NONE', *, *, #20066, .F. ) ;
#18558=CARTESIAN_POINT ( 'NONE',  ( -0.1377952755905511861, -1.331775896911328393E-15, -0.8070866141732283561 ) ) ;
#18807=CARTESIAN_POINT ( 'NONE',  ( -0.4330708661417345673, 3.105646754637360326E-15, -0.9891732283464566011 ) ) ;
#18848=DIRECTION ( 'NONE',  ( 1.144917494144692682E-16, -3.972230510298676574E-31, 1.000000000000000000 ) ) ;
#18911=DIRECTION ( 'NONE',  ( -3.469446951953613794E-15, -1.000000000000000000, -1.118797478067273468E-31 ) ) ;
#18943=( NAMED_UNIT ( * ) PLANE_ANGLE_UNIT ( ) SI_UNIT ( $, .RADIAN. ) ) ;
#19123=CARTESIAN_POINT ( 'NONE',  ( -0.4330708661417340677, 0.1574803149606330277, -0.9891732283464564901 ) ) ;
#19257=CONICAL_SURFACE ( 'NONE', #36884, 0.1003937007874010356, 0.7853981633978647237 ) ;
#19612=ORIENTED_EDGE ( 'NONE', *, *, #21912, .F. ) ;
#19797=CARTESIAN_POINT ( 'NONE',  ( -0.1377952755905511861, 0.1574803149606320007, 0.8070866141732283561 ) ) ;
#19941=AXIS2_PLACEMENT_3D ( 'NONE', #20936, #42496, #28887 ) ;
#19950=EDGE_CURVE ( 'NONE', #32133, #3713, #17674, .T. ) ;
#20050=AXIS2_PLACEMENT_3D ( 'NONE', #26221, #33655, #26459 ) ;
#20066=EDGE_CURVE ( 'NONE', #24265, #41049, #47153, .T. ) ;
#20125=EDGE_CURVE ( 'NONE', #17766, #28143, #43641, .T. ) ;
#20130=AXIS2_PLACEMENT_3D ( 'NONE', #17669, #43054, #20554 ) ;
#20154=CARTESIAN_POINT ( 'NONE',  ( 0.4620708661417356478, 0.9842519685039370358, -0.7135826771653542844 ) ) ;
#20235=DIRECTION ( 'NONE',  ( 3.469446951953613794E-15, 1.000000000000000000, 0.000000000000000000 ) ) ;
#20354=EDGE_CURVE ( 'NONE', #37817, #4137, #1600, .T. ) ;
#20406=ADVANCED_FACE ( 'NONE', ( #13555 ), #41574, .F. ) ;
#20532=ORIENTED_EDGE ( 'NONE', *, *, #31462, .F. ) ;
#20551=LINE ( 'NONE', #35427, #38352 ) ;
#20554=DIRECTION ( 'NONE',  ( 1.000000000000000000, -3.368395098984090098E-15, 0.000000000000000000 ) ) ;
#20698=CARTESIAN_POINT ( 'NONE',  ( 0.4330708661417289052, 1.006139616066741879E-16, -1.186023622047243986 ) ) ;
#20829=ORIENTED_EDGE ( 'NONE', *, *, #106, .F. ) ;
#20860=AXIS2_PLACEMENT_3D ( 'NONE', #25692, #32652, #10835 ) ;
#20891=FACE_OUTER_BOUND ( 'NONE', #11025, .T. ) ;
#20936=CARTESIAN_POINT ( 'NONE',  ( -0.1377952755905511861, 0.1564960629921283985, 0.8070866141732283561 ) ) ;
#20939=AXIS2_PLACEMENT_3D ( 'NONE', #15619, #40502, #15375 ) ;
#20964=ORIENTED_EDGE ( 'NONE', *, *, #40609, .T. ) ;
#21021=CIRCLE ( 'NONE', #14175, 0.02900000000000001882 ) ;
#21094=VECTOR ( 'NONE', #28711, 39.37007874015748143 ) ;
#21220=ORIENTED_EDGE ( 'NONE', *, *, #16650, .F. ) ;
#21227=VERTEX_POINT ( 'NONE', #24950 ) ;
#21242=VECTOR ( 'NONE', #13499, 39.37007874015748143 ) ;
#21419=DIRECTION ( 'NONE',  ( 0.000000000000000000, 0.000000000000000000, 1.000000000000000000 ) ) ;
#21468=ORIENTED_EDGE ( 'NONE', *, *, #15135, .F. ) ;
#21477=VERTEX_POINT ( 'NONE', #14881 ) ;
#21533=CARTESIAN_POINT ( 'NONE',  ( -0.1377952755905511861, -1.331775896911328393E-15, 0.8070866141732283561 ) ) ;
#21619=( CONVERSION_BASED_UNIT ( 'INCH', #28605 ) LENGTH_UNIT ( ) NAMED_UNIT ( #16385 ) ) ;
#21647=ADVANCED_FACE ( 'NONE', ( #28488 ), #19257, .F. ) ;
#21762=ORIENTED_EDGE ( 'NONE', *, *, #20354, .T. ) ;
#21789=AXIS2_PLACEMENT_3D ( 'NONE', #14387, #29036, #43836 ) ;
#21912=EDGE_CURVE ( 'NONE', #25198, #1966, #7064, .T. ) ;
#21917=DIRECTION ( 'NONE',  ( -1.000000000000000000, 3.469446951953614189E-15, 1.144917494144692682E-16 ) ) ;
#21956=LINE ( 'NONE', #15250, #27485 ) ;
#21960=CARTESIAN_POINT ( 'NONE',  ( -0.1377952755905511861, 0.1574803149606320007, -0.8070866141732283561 ) ) ;
#21974=EDGE_CURVE ( 'NONE', #45730, #3713, #33683, .T. ) ;
#22011=VERTEX_POINT ( 'NONE', #44408 ) ;
#22082=EDGE_CURVE ( 'NONE', #3381, #39582, #23099, .T. ) ;
#22084=( NAMED_UNIT ( * ) PLANE_ANGLE_UNIT ( ) SI_UNIT ( $, .RADIAN. ) ) ;
#22088=CARTESIAN_POINT ( 'NONE',  ( -0.2362204724409471546, 2.422684756221294423E-15, -0.9891732283464564901 ) ) ;
#22108=PRODUCT_DEFINITION_CONTEXT ( 'detailed design', #12884, 'design' ) ;
#22129=DIRECTION ( 'NONE',  ( 0.000000000000000000, 1.000000000000000000, 0.000000000000000000 ) ) ;
#22177=ORIENTED_EDGE ( 'NONE', *, *, #25029, .T. ) ;
#22193=DIRECTION ( 'NONE',  ( -1.000000000000000000, 3.469446951953613794E-15, 1.144917494144692682E-16 ) ) ;
#22200=LINE ( 'NONE', #4213, #8593 ) ;
#22258=CARTESIAN_POINT ( 'NONE',  ( -0.2362204724409466272, 0.1574803149606323616, -1.186023622047243986 ) ) ;
#22314=CARTESIAN_POINT ( 'NONE',  ( -0.1377952755905511584, -1.331775896911328393E-15, -0.9074803149606294195 ) ) ;
#22385=DIRECTION ( 'NONE',  ( 1.000000000000000000, 0.000000000000000000, -1.144917494144692682E-16 ) ) ;
#22446=ADVANCED_FACE ( 'NONE', ( #17559, #47025, #32197 ), #28621, .F. ) ;
#22492=ORIENTED_EDGE ( 'NONE', *, *, #42976, .F. ) ;
#22502=ORIENTED_EDGE ( 'NONE', *, *, #37774, .T. ) ;
#22512=PLANE ( 'NONE',  #26020 ) ;
#22695=CYLINDRICAL_SURFACE ( 'NONE', #35228, 0.02900000000000001882 ) ;
#22841=CARTESIAN_POINT ( 'NONE',  ( -0.1377952755905511861, 0.1574803149606320007, 0.8070866141732283561 ) ) ;
#22865=VECTOR ( 'NONE', #12664, 39.37007874015748143 ) ;
#22876=VERTEX_POINT ( 'NONE', #12522 ) ;
#22920=DIRECTION ( 'NONE',  ( -1.000000000000000000, 3.469446951953614189E-15, 1.144917494144692682E-16 ) ) ;
#22932=FACE_OUTER_BOUND ( 'NONE', #16934, .T. ) ;
#22935=CARTESIAN_POINT ( 'NONE',  ( 0.4330708661417329020, 0.1864803149606300281, -1.186023622047243986 ) ) ;
#23081=CYLINDRICAL_SURFACE ( 'NONE', #1676, 0.1003937007874010356 ) ;
#23099=CIRCLE ( 'NONE', #3179, 0.1003937007874010356 ) ;
#23143=CONICAL_SURFACE ( 'NONE', #1701, 0.1003937007874010356, 0.7853981633978647237 ) ;
#23159=FACE_OUTER_BOUND ( 'NONE', #43197, .T. ) ;
#23180=DIRECTION ( 'NONE',  ( -1.000000000000000000, 0.000000000000000000, 0.000000000000000000 ) ) ;
#23244=ORIENTED_EDGE ( 'NONE', *, *, #8398, .T. ) ;
#23442=ORIENTED_EDGE ( 'NONE', *, *, #44195, .F. ) ;
#23843=DIRECTION ( 'NONE',  ( 1.151683635503274272E-16, -4.091602205503172741E-31, 1.000000000000000000 ) ) ;
#23867=DIRECTION ( 'NONE',  ( -3.469446951953614189E-15, -1.000000000000000000, 0.000000000000000000 ) ) ;
#23906=ORIENTED_EDGE ( 'NONE', *, *, #3583, .F. ) ;
#23939=CARTESIAN_POINT ( 'NONE',  ( 0.4620708661417356478, 0.9842519685039370358, -0.7135826771653542844 ) ) ;
#23977=ORIENTED_EDGE ( 'NONE', *, *, #27598, .F. ) ;
#23992=VECTOR ( 'NONE', #29031, 39.37007874015748143 ) ;
#24032=EDGE_CURVE ( 'NONE', #17766, #28233, #34792, .T. ) ;
#24038=CARTESIAN_POINT ( 'NONE',  ( 0.6195511811023612925, 0.6102362204724401940, 1.186023622047243986 ) ) ;
#24057=ORIENTED_EDGE ( 'NONE', *, *, #18300, .F. ) ;
#24162=DIRECTION ( 'NONE',  ( 0.000000000000000000, 0.000000000000000000, 1.000000000000000000 ) ) ;
#24170=AXIS2_PLACEMENT_3D ( 'NONE', #4968, #29721, #44496 ) ;
#24214=EDGE_CURVE ( 'NONE', #5872, #36671, #35494, .T. ) ;
#24265=VERTEX_POINT ( 'NONE', #14582 ) ;
#24352=ORIENTED_EDGE ( 'NONE', *, *, #33471, .T. ) ;
#24415=EDGE_CURVE ( 'NONE', #39582, #30632, #41356, .T. ) ;
#24467=DIRECTION ( 'NONE',  ( -3.469446951953613794E-15, -1.000000000000000000, 0.000000000000000000 ) ) ;
#24531=PLANE ( 'NONE',  #28183 ) ;
#24592=ORIENTED_EDGE ( 'NONE', *, *, #11122, .F. ) ;
#24596=ORIENTED_EDGE ( 'NONE', *, *, #14353, .F. ) ;
#24706=CARTESIAN_POINT ( 'NONE',  ( -0.1377952755905511584, 0.1564960629921283985, 0.7066929133858274037 ) ) ;
#24748=ORIENTED_EDGE ( 'NONE', *, *, #3903, .T. ) ;
#24854=CARTESIAN_POINT ( 'NONE',  ( -0.1377952755905511861, 0.1564960629921283985, -0.8070866141732283561 ) ) ;
#24950=CARTESIAN_POINT ( 'NONE',  ( 0.6195511811023624027, 0.9842519685039370358, -0.8759842519685050455 ) ) ;
#24964=ORIENTED_EDGE ( 'NONE', *, *, #34067, .T. ) ;
#25029=EDGE_CURVE ( 'NONE', #15018, #22876, #7172, .T. ) ;
#25036=LINE ( 'NONE', #7302, #37312 ) ;
#25080=CARTESIAN_POINT ( 'NONE',  ( -0.2362204724409469048, 2.422684756221293634E-15, 1.186023622047244208 ) ) ;
#25160=LINE ( 'NONE', #43111, #23992 ) ;
#25194=DIRECTION ( 'NONE',  ( 1.144917494144692682E-16, -3.972230510298674823E-31, 1.000000000000000000 ) ) ;
#25198=VERTEX_POINT ( 'NONE', #19123 ) ;
#25213=( NAMED_UNIT ( * ) SI_UNIT ( $, .STERADIAN. ) SOLID_ANGLE_UNIT ( ) ) ;
#25277=CYLINDRICAL_SURFACE ( 'NONE', #47033, 0.1968503937007874127 ) ;
#25302=DIRECTION ( 'NONE',  ( 3.469446951953615767E-15, 1.000000000000000000, 0.000000000000000000 ) ) ;
#25341=ADVANCED_FACE ( 'NONE', ( #5212 ), #45220, .T. ) ;
#25390=EDGE_LOOP ( 'NONE', ( #17406, #25855, #23977, #44857 ) ) ;
#25436=STYLED_ITEM ( 'NONE', ( #46958 ), #36893 ) ;
#25460=( LENGTH_UNIT ( ) NAMED_UNIT ( * ) SI_UNIT ( $, .METRE. ) ) ;
#25475=DIRECTION ( 'NONE',  ( 1.000000000000000000, -3.469446951953614189E-15, 0.000000000000000000 ) ) ;
#25522=ORIENTED_EDGE ( 'NONE', *, *, #25029, .F. ) ;
#25529=VECTOR ( 'NONE', #9219, 39.37007874015748143 ) ;
#25574=FACE_OUTER_BOUND ( 'NONE', #30475, .T. ) ;
#25644=FACE_OUTER_BOUND ( 'NONE', #39760, .T. ) ;
#25692=CARTESIAN_POINT ( 'NONE',  ( 0.000000000000000000, 0.000000000000000000, 0.000000000000000000 ) ) ;
#25713=CIRCLE ( 'NONE', #37911, 0.1003937007874010356 ) ;
#25772=EDGE_CURVE ( 'NONE', #2262, #3336, #7580, .T. ) ;
#25852=CIRCLE ( 'NONE', #8213, 0.1624015748031507056 ) ;
#25855=ORIENTED_EDGE ( 'NONE', *, *, #46636, .F. ) ;
#25872=CARTESIAN_POINT ( 'NONE',  ( -0.1377952755905511861, 0.1574803149606320007, 0.8070866141732283561 ) ) ;
#26020=AXIS2_PLACEMENT_3D ( 'NONE', #37128, #18911, #33568 ) ;
#26032=ORIENTED_EDGE ( 'NONE', *, *, #37271, .T. ) ;
#26112=DIRECTION ( 'NONE',  ( 1.000000000000000000, -3.469446951953614189E-15, 0.000000000000000000 ) ) ;
#26221=CARTESIAN_POINT ( 'NONE',  ( -0.1377952755905511861, 0.1564960629921283985, 0.8070866141732283561 ) ) ;
#26269=ADVANCED_FACE ( 'NONE', ( #17841 ), #25277, .T. ) ;
#26414=LINE ( 'NONE', #496, #36132 ) ;
#26459=DIRECTION ( 'NONE',  ( 0.000000000000000000, 0.000000000000000000, 1.000000000000000000 ) ) ;
#26493=CARTESIAN_POINT ( 'NONE',  ( 0.6195511811023624027, 0.9842519685039365918, -0.7135826771653542844 ) ) ;
#26502=UNCERTAINTY_MEASURE_WITH_UNIT (LENGTH_MEASURE( 1.000000000000000082E-05 ), #15376, 'distance_accuracy_value', 'NONE') ;
#26544=ORIENTED_EDGE ( 'NONE', *, *, #11655, .F. ) ;
#26573=LINE ( 'NONE', #37320, #5782 ) ;
#26599=FACE_OUTER_BOUND ( 'NONE', #41146, .T. ) ;
#26622=VECTOR ( 'NONE', #41289, 39.37007874015748854 ) ;
#26718=AXIS2_PLACEMENT_3D ( 'NONE', #1596, #31110, #5439 ) ;
#26736=CARTESIAN_POINT ( 'NONE',  ( 0.4620708661417344820, 0.6102362204724408601, 0.5167322834645649010 ) ) ;
#26738=ORIENTED_EDGE ( 'NONE', *, *, #21974, .F. ) ;
#26760=EDGE_CURVE ( 'NONE', #8777, #25198, #38116, .T. ) ;
#26865=EDGE_CURVE ( 'NONE', #40961, #21477, #46513, .T. ) ;
#26929=ORIENTED_EDGE ( 'NONE', *, *, #22082, .F. ) ;
#26981=EDGE_CURVE ( 'NONE', #36211, #42479, #16738, .T. ) ;
#26989=AXIS2_PLACEMENT_3D ( 'NONE', #41390, #8590, #31143 ) ;
#27049=PLANE ( 'NONE',  #43218 ) ;
#27056=VECTOR ( 'NONE', #35018, 39.37007874015748854 ) ;
#27060=CIRCLE ( 'NONE', #6359, 0.4724409448818900348 ) ;
#27085=VECTOR ( 'NONE', #32376, 39.37007874015748143 ) ;
#27096=ORIENTED_EDGE ( 'NONE', *, *, #31462, .T. ) ;
#27125=CARTESIAN_POINT ( 'NONE',  ( -0.1377952755905511861, -1.331775896911328393E-15, -0.8070866141732283561 ) ) ;
#27218=CARTESIAN_POINT ( 'NONE',  ( -0.1377952755905511584, 0.1564960629921283985, -0.9074803149606294195 ) ) ;
#27257=DIRECTION ( 'NONE',  ( -3.469446951953614189E-15, -1.000000000000000000, 0.000000000000000000 ) ) ;
#27314=ORIENTED_EDGE ( 'NONE', *, *, #10785, .F. ) ;
#27340=ORIENTED_EDGE ( 'NONE', *, *, #3195, .T. ) ;
#27462=VERTEX_POINT ( 'NONE', #40863 ) ;
#27470=CARTESIAN_POINT ( 'NONE',  ( 0.6195511811023618476, 0.8070866141732275789, 0.5854071585544579071 ) ) ;
#27473=ORIENTED_EDGE ( 'NONE', *, *, #40609, .F. ) ;
#27485=VECTOR ( 'NONE', #44439, 39.37007874015748143 ) ;
#27495=DIRECTION ( 'NONE',  ( -1.144917494144692682E-16, 5.091027988365947196E-31, -1.000000000000000000 ) ) ;
#27497=CARTESIAN_POINT ( 'NONE',  ( -0.1377952755905511584, 0.1574803149606320007, -0.9084645669291337988 ) ) ;
#27598=EDGE_CURVE ( 'NONE', #22876, #32133, #36642, .T. ) ;
#27644=ORIENTED_EDGE ( 'NONE', *, *, #11875, .F. ) ;
#27702=EDGE_LOOP ( 'NONE', ( #186, #5371, #24352, #17147 ) ) ;
#27733=CARTESIAN_POINT ( 'NONE',  ( 0.4620708661417328167, 0.1864803149606299448, -0.7135826771653542844 ) ) ;
#27776=DIRECTION ( 'NONE',  ( 0.000000000000000000, -0.6220299971367093672, 0.7829934116339072325 ) ) ;
#27780=VERTEX_POINT ( 'NONE', #27497 ) ;
#27835=ORIENTED_EDGE ( 'NONE', *, *, #6591, .F. ) ;
#27868=ORIENTED_EDGE ( 'NONE', *, *, #26760, .T. ) ;
#27933=LINE ( 'NONE', #46573, #6053 ) ;
#27956=DIRECTION ( 'NONE',  ( 1.144917494144692682E-16, 2.347476851301873061E-33, 1.000000000000000000 ) ) ;
#28143=VERTEX_POINT ( 'NONE', #14268 ) ;
#28183=AXIS2_PLACEMENT_3D ( 'NONE', #39131, #6302, #46557 ) ;
#28233=VERTEX_POINT ( 'NONE', #40109 ) ;
#28291=CIRCLE ( 'NONE', #40527, 0.1968503937007874405 ) ;
#28297=FILL_AREA_STYLE ('',( #17026 ) ) ;
#28334=CARTESIAN_POINT ( 'NONE',  ( 0.4620708661417327612, 0.1864803149606299448, -1.186023622047243986 ) ) ;
#28338=DIRECTION ( 'NONE',  ( -1.000000000000000000, 0.000000000000000000, 0.000000000000000000 ) ) ;
#28368=DIRECTION ( 'NONE',  ( 1.000000000000000000, -3.469446951953614978E-15, 0.000000000000000000 ) ) ;
#28488=FACE_OUTER_BOUND ( 'NONE', #39486, .T. ) ;
#28514=CARTESIAN_POINT ( 'NONE',  ( -0.1377952755905511861, 0.1564960629921283985, -0.7066929133858274037 ) ) ;
#28539=PLANE ( 'NONE',  #41364 ) ;
#28546=SURFACE_SIDE_STYLE ('',( #31663 ) ) ;
#28605=LENGTH_MEASURE_WITH_UNIT ( LENGTH_MEASURE( 0.02539999999999999897 ), #3871 ) ;
#28621=PLANE ( 'NONE',  #1702 ) ;
#28711=DIRECTION ( 'NONE',  ( -3.469446951953614583E-15, -1.000000000000000000, -1.751623080406021339E-46 ) ) ;
#28735=AXIS2_PLACEMENT_3D ( 'NONE', #21533, #36170, #3325 ) ;
#28887=DIRECTION ( 'NONE',  ( 0.000000000000000000, 0.000000000000000000, -1.000000000000000000 ) ) ;
#28903=DIRECTION ( 'NONE',  ( -3.469446951953614189E-15, -1.000000000000000000, 0.000000000000000000 ) ) ;
#28925=CARTESIAN_POINT ( 'NONE',  ( 0.6195511811023590720, -5.463695987328343027E-16, 1.186023622047243986 ) ) ;
#29013=ORIENTED_EDGE ( 'NONE', *, *, #31842, .T. ) ;
#29031=DIRECTION ( 'NONE',  ( -1.144917494144692682E-16, -2.347476851301873745E-33, -1.000000000000000000 ) ) ;
#29036=DIRECTION ( 'NONE',  ( -1.144917494144692682E-16, 3.972230510298676574E-31, -1.000000000000000000 ) ) ;
#29175=AXIS2_PLACEMENT_3D ( 'NONE', #33978, #18848, #37538 ) ;
#29185=CIRCLE ( 'NONE', #19941, 0.1003937007874010356 ) ;
#29283=DIRECTION ( 'NONE',  ( -3.469446951953614978E-15, -1.000000000000000000, 3.995705278811693553E-31 ) ) ;
#29349=( GEOMETRIC_REPRESENTATION_CONTEXT ( 3 ) GLOBAL_UNCERTAINTY_ASSIGNED_CONTEXT ( ( #26502 ) ) GLOBAL_UNIT_ASSIGNED_CONTEXT ( ( #15376, #18943, #37393 ) ) REPRESENTATION_CONTEXT ( 'NONE', 'WORKASPACE' ) ) ;
#29423=LINE ( 'NONE', #28925, #40712 ) ;
#29455=CIRCLE ( 'NONE', #4136, 0.1003937007874010356 ) ;
#29721=DIRECTION ( 'NONE',  ( 3.469446951953614583E-15, 1.000000000000000000, 0.000000000000000000 ) ) ;
#29744=AXIS2_PLACEMENT_3D ( 'NONE', #15097, #47441, #26112 ) ;
#29809=ADVANCED_FACE ( 'NONE', ( #7895, #40933, #40698 ), #22512, .T. ) ;
#29933=ORIENTED_EDGE ( 'NONE', *, *, #19950, .F. ) ;
#29936=EDGE_LOOP ( 'NONE', ( #30993, #16248, #38087, #38960 ) ) ;
#30064=ORIENTED_EDGE ( 'NONE', *, *, #30443, .F. ) ;
#30156=DIRECTION ( 'NONE',  ( 1.000000000000000000, -3.469446951953614189E-15, -1.144917494144692682E-16 ) ) ;
#30162=ORIENTED_EDGE ( 'NONE', *, *, #40238, .T. ) ;
#30186=CARTESIAN_POINT ( 'NONE',  ( 0.6195511811023604043, 0.4133858267716528090, 1.186023622047243986 ) ) ;
#30267=DIRECTION ( 'NONE',  ( 1.000000000000000000, -0.000000000000000000, -1.144917494144692682E-16 ) ) ;
#30309=FACE_OUTER_BOUND ( 'NONE', #38970, .T. ) ;
#30345=PRODUCT_DEFINITION_SHAPE ( 'NONE', 'NONE',  #14855 ) ;
#30376=AXIS2_PLACEMENT_3D ( 'NONE', #18102, #43253, #32020 ) ;
#30443=EDGE_CURVE ( 'NONE', #13083, #36338, #41111, .T. ) ;
#30475=EDGE_LOOP ( 'NONE', ( #14184, #4656, #44375, #27473 ) ) ;
#30484=ADVANCED_FACE ( 'NONE', ( #33984 ), #22695, .F. ) ;
#30526=EDGE_LOOP ( 'NONE', ( #21220, #30162, #11050, #32882 ) ) ;
#30565=ORIENTED_EDGE ( 'NONE', *, *, #34773, .T. ) ;
#30608=CARTESIAN_POINT ( 'NONE',  ( 0.6195511811023606263, 0.4133858267716528090, 0.9891732283464566011 ) ) ;
#30632=VERTEX_POINT ( 'NONE', #16924 ) ;
#30859=VERTEX_POINT ( 'NONE', #3491 ) ;
#30888=EDGE_CURVE ( 'NONE', #36211, #4000, #45931, .T. ) ;
#30952=DIRECTION ( 'NONE',  ( -0.000000000000000000, 1.000000000000000000, -3.995705278811693553E-31 ) ) ;
#30993=ORIENTED_EDGE ( 'NONE', *, *, #34866, .F. ) ;
#31089=ORIENTED_EDGE ( 'NONE', *, *, #31842, .F. ) ;
#31110=DIRECTION ( 'NONE',  ( 0.000000000000000000, 1.000000000000000000, 0.000000000000000000 ) ) ;
#31143=DIRECTION ( 'NONE',  ( -3.469446951953613794E-15, -1.000000000000000000, 0.000000000000000000 ) ) ;
#31187=CARTESIAN_POINT ( 'NONE',  ( 0.4330708661417291827, 1.006139616066729676E-16, 1.186023622047243986 ) ) ;
#31192=CARTESIAN_POINT ( 'NONE',  ( -0.1377952755905511861, 0.1574803149606320007, -0.7057086614173230243 ) ) ;
#31206=FACE_OUTER_BOUND ( 'NONE', #44471, .T. ) ;
#31428=VECTOR ( 'NONE', #11215, 39.37007874015748143 ) ;
#31462=EDGE_CURVE ( 'NONE', #1966, #3336, #32219, .T. ) ;
#31585=DIRECTION ( 'NONE',  ( 2.787771407953479926E-15, 0.7829934116339072325, 0.6220299971367093672 ) ) ;
#31661=DIRECTION ( 'NONE',  ( 1.000000000000000000, -3.469446951953614189E-15, -1.144917494144692682E-16 ) ) ;
#31663=SURFACE_STYLE_FILL_AREA ( #28297 ) ;
#31742=EDGE_CURVE ( 'NONE', #36338, #41049, #6935, .T. ) ;
#31792=DIRECTION ( 'NONE',  ( 3.469446951953614978E-15, 1.000000000000000000, -3.995705278811693553E-31 ) ) ;
#31816=DIRECTION ( 'NONE',  ( 1.000000000000000000, -3.368395098984090098E-15, 0.000000000000000000 ) ) ;
#31842=EDGE_CURVE ( 'NONE', #4000, #36211, #41355, .T. ) ;
#31934=DIRECTION ( 'NONE',  ( -1.144917494144692682E-16, 3.972230510298674823E-31, -1.000000000000000000 ) ) ;
#31935=CARTESIAN_POINT ( 'NONE',  ( 0.6195511811023624027, 0.9842519685039370358, -0.7135826771653542844 ) ) ;
#31983=CYLINDRICAL_SURFACE ( 'NONE', #24170, 0.1968503937007874405 ) ;
#32020=DIRECTION ( 'NONE',  ( 0.000000000000000000, 0.000000000000000000, -1.000000000000000000 ) ) ;
#32070=AXIS2_PLACEMENT_3D ( 'NONE', #8291, #45646, #27257 ) ;
#32120=DIRECTION ( 'NONE',  ( -3.469446951953613794E-15, -1.000000000000000000, 0.000000000000000000 ) ) ;
#32133=VERTEX_POINT ( 'NONE', #42991 ) ;
#32197=FACE_OUTER_BOUND ( 'NONE', #39652, .T. ) ;
#32219=CIRCLE ( 'NONE', #12299, 0.1968503937007874127 ) ;
#32356=ORIENTED_EDGE ( 'NONE', *, *, #6591, .T. ) ;
#32376=DIRECTION ( 'NONE',  ( 2.055777091826793380E-15, 0.6220299971367094782, -0.7829934116339072325 ) ) ;
#32422=PRODUCT_DEFINITION_FORMATION_WITH_SPECIFIED_SOURCE ( 'ANY', '', #33371, .NOT_KNOWN. ) ;
#32534=CARTESIAN_POINT ( 'NONE',  ( 0.6195511811023595161, 0.1864803149606293897, -1.186023622047243986 ) ) ;
#32595=ORIENTED_EDGE ( 'NONE', *, *, #34773, .F. ) ;
#32652=DIRECTION ( 'NONE',  ( 0.000000000000000000, 0.000000000000000000, 1.000000000000000000 ) ) ;
#32735=CARTESIAN_POINT ( 'NONE',  ( -0.4330708661417345673, 3.105646754637360326E-15, -0.9891732283464564901 ) ) ;
#32795=CYLINDRICAL_SURFACE ( 'NONE', #45275, 0.1968503937007874127 ) ;
#32844=DIRECTION ( 'NONE',  ( 0.000000000000000000, 1.000000000000000000, 0.000000000000000000 ) ) ;
#32882=ORIENTED_EDGE ( 'NONE', *, *, #9376, .F. ) ;
#32885=ORIENTED_EDGE ( 'NONE', *, *, #30888, .F. ) ;
#32969=DIRECTION ( 'NONE',  ( 0.000000000000000000, 0.000000000000000000, 1.000000000000000000 ) ) ;
#33040=UNCERTAINTY_MEASURE_WITH_UNIT (LENGTH_MEASURE( 1.000000000000000082E-05 ), #21619, 'distance_accuracy_value', 'NONE') ;
#33233=AXIS2_PLACEMENT_3D ( 'NONE', #31935, #46523, #6505 ) ;
#33278=DIRECTION ( 'NONE',  ( 0.000000000000000000, 0.000000000000000000, 1.000000000000000000 ) ) ;
#33371=PRODUCT ( 'Side Bracket', 'Side Bracket', '', ( #42452 ) ) ;
#33419=EDGE_LOOP ( 'NONE', ( #7035, #23906, #12108, #3364 ) ) ;
#33446=CARTESIAN_POINT ( 'NONE',  ( 0.6195511811023590720, -5.463695987328343027E-16, 1.186023622047243986 ) ) ;
#33471=EDGE_CURVE ( 'NONE', #4000, #21227, #26414, .T. ) ;
#33478=DIRECTION ( 'NONE',  ( -0.000000000000000000, 1.000000000000000000, -3.995705278811693553E-31 ) ) ;
#33506=CARTESIAN_POINT ( 'NONE',  ( 0.6195511811023624027, 0.9842519685039370358, -0.7135826771653542844 ) ) ;
#33568=DIRECTION ( 'NONE',  ( 1.000000000000000000, -3.469446951953613794E-15, 0.000000000000000000 ) ) ;
#33655=DIRECTION ( 'NONE',  ( 0.000000000000000000, 1.000000000000000000, 0.000000000000000000 ) ) ;
#33683=LINE ( 'NONE', #7770, #44519 ) ;
#33702=DIRECTION ( 'NONE',  ( 1.000000000000000000, -3.368395098984090098E-15, 0.000000000000000000 ) ) ;
#33720=ORIENTED_EDGE ( 'NONE', *, *, #6320, .F. ) ;
#33737=VECTOR ( 'NONE', #10755, 39.37007874015748143 ) ;
#33745=ADVANCED_FACE ( 'NONE', ( #10264 ), #32795, .T. ) ;
#33781=ORIENTED_EDGE ( 'NONE', *, *, #3376, .T. ) ;
#33799=DIRECTION ( 'NONE',  ( 3.469446951953614583E-15, 1.000000000000000000, -0.000000000000000000 ) ) ;
#33832=ORIENTED_EDGE ( 'NONE', *, *, #18300, .T. ) ;
#33863=VECTOR ( 'NONE', #33799, 39.37007874015748143 ) ;
#33978=CARTESIAN_POINT ( 'NONE',  ( 0.4330708661417297933, 0.1864803149606300281, 1.186023622047243986 ) ) ;
#33984=FACE_OUTER_BOUND ( 'NONE', #33419, .T. ) ;
#34067=EDGE_CURVE ( 'NONE', #3336, #8777, #11031, .T. ) ;
#34127=DIRECTION ( 'NONE',  ( -0.000000000000000000, 1.000000000000000000, -3.995705278811693553E-31 ) ) ;
#34152=CARTESIAN_POINT ( 'NONE',  ( 0.6195511811023604043, 0.4133858267716528090, 1.186023622047243986 ) ) ;
#34230=CARTESIAN_POINT ( 'NONE',  ( -0.1377952755905511584, 0.1574803149606320007, -0.9074803149606294195 ) ) ;
#34271=ADVANCED_FACE ( 'NONE', ( #9319, #26599 ), #41872, .F. ) ;
#34424=DIRECTION ( 'NONE',  ( -3.364312195833787750E-15, -1.000000000000000000, 0.000000000000000000 ) ) ;
#34450=LINE ( 'NONE', #30186, #22865 ) ;
#34673=DIRECTION ( 'NONE',  ( 1.000000000000000000, -3.469446951953614189E-15, 6.938893903907228378E-16 ) ) ;
#34687=AXIS2_PLACEMENT_3D ( 'NONE', #24038, #1079, #35057 ) ;
#34714=EDGE_CURVE ( 'NONE', #27780, #36671, #39186, .T. ) ;
#34770=CARTESIAN_POINT ( 'NONE',  ( -0.2362204724409467105, 0.1574803149606323616, -1.186023622047243986 ) ) ;
#34773=EDGE_CURVE ( 'NONE', #28143, #3083, #29423, .T. ) ;
#34792=LINE ( 'NONE', #45530, #15521 ) ;
#34849=ORIENTED_EDGE ( 'NONE', *, *, #44195, .T. ) ;
#34866=EDGE_CURVE ( 'NONE', #30859, #36338, #5613, .T. ) ;
#34907=LINE ( 'NONE', #27733, #43026 ) ;
#35018=DIRECTION ( 'NONE',  ( 0.000000000000000000, 0.7071067811862530306, 0.7071067811868418929 ) ) ;
#35054=VECTOR ( 'NONE', #9627, 39.37007874015748143 ) ;
#35057=DIRECTION ( 'NONE',  ( -1.000000000000000000, 3.469446951953613794E-15, 0.000000000000000000 ) ) ;
#35219=ORIENTED_EDGE ( 'NONE', *, *, #26865, .F. ) ;
#35228=AXIS2_PLACEMENT_3D ( 'NONE', #22935, #1110, #23180 ) ;
#35382=EDGE_LOOP ( 'NONE', ( #24592, #16471, #42017, #1171 ) ) ;
#35427=CARTESIAN_POINT ( 'NONE',  ( 0.4620708661417355922, 0.9842519685039370358, -1.186023622047243986 ) ) ;
#35487=SURFACE_STYLE_USAGE ( .BOTH. , #28546 ) ;
#35494=LINE ( 'NONE', #42867, #27056 ) ;
#35532=CYLINDRICAL_SURFACE ( 'NONE', #33233, 0.1624015748031507056 ) ;
#35548=ORIENTED_EDGE ( 'NONE', *, *, #20354, .F. ) ;
#35618=CARTESIAN_POINT ( 'NONE',  ( 0.4620708661417356478, 0.9842519685039370358, -0.7135826771653542844 ) ) ;
#35651=ORIENTED_EDGE ( 'NONE', *, *, #4417, .T. ) ;
#35802=VECTOR ( 'NONE', #40009, 39.37007874015748143 ) ;
#35937=CARTESIAN_POINT ( 'NONE',  ( 0.6195511811023621807, 0.9842519685039365918, -1.186023622047243986 ) ) ;
#36132=VECTOR ( 'NONE', #30267, 39.37007874015748143 ) ;
#36170=DIRECTION ( 'NONE',  ( -0.000000000000000000, 1.000000000000000000, -3.995705278811693553E-31 ) ) ;
#36173=AXIS2_PLACEMENT_3D ( 'NONE', #18342, #7324, #33702 ) ;
#36211=VERTEX_POINT ( 'NONE', #41495 ) ;
#36338=VERTEX_POINT ( 'NONE', #17311 ) ;
#36427=ORIENTED_EDGE ( 'NONE', *, *, #554, .T. ) ;
#36434=ORIENTED_EDGE ( 'NONE', *, *, #554, .F. ) ;
#36470=DIRECTION ( 'NONE',  ( 1.000000000000000000, -3.469446951953613794E-15, -1.144917494144692682E-16 ) ) ;
#36520=EDGE_LOOP ( 'NONE', ( #14745, #30064, #1010, #16008 ) ) ;
#36642=CIRCLE ( 'NONE', #32070, 0.1968503937007874127 ) ;
#36671=VERTEX_POINT ( 'NONE', #31192 ) ;
#36815=ORIENTED_EDGE ( 'NONE', *, *, #3195, .F. ) ;
#36884=AXIS2_PLACEMENT_3D ( 'NONE', #10263, #10982, #3289 ) ;
#36893=MANIFOLD_SOLID_BREP ( 'Side Bracket', #13265 ) ;
#37040=DIRECTION ( 'NONE',  ( -0.000000000000000000, 1.000000000000000000, -3.995705278811693553E-31 ) ) ;
#37072=CARTESIAN_POINT ( 'NONE',  ( 0.6195511811023636239, 1.354170115732554747, -0.4197102375732078561 ) ) ;
#37076=EDGE_LOOP ( 'NONE', ( #24748, #43777 ) ) ;
#37128=CARTESIAN_POINT ( 'NONE',  ( 0.6195511811023588500, -5.463695987328330208E-16, -1.186023622047243986 ) ) ;
#37250=DIRECTION ( 'NONE',  ( -1.000000000000000000, 3.469446951953614189E-15, 1.144917494144692682E-16 ) ) ;
#37271=EDGE_CURVE ( 'NONE', #38595, #8725, #25160, .T. ) ;
#37288=VECTOR ( 'NONE', #1513, 39.37007874015748143 ) ;
#37297=CARTESIAN_POINT ( 'NONE',  ( 0.4330708661417327909, 0.1574803149606300301, 1.186023622047243986 ) ) ;
#37312=VECTOR ( 'NONE', #14733, 39.37007874015748854 ) ;
#37320=CARTESIAN_POINT ( 'NONE',  ( -0.1377952755905511861, 0.1574803149606320007, 0.9074803149606294195 ) ) ;
#37325=EDGE_CURVE ( 'NONE', #894, #13083, #39989, .T. ) ;
#37330=ORIENTED_EDGE ( 'NONE', *, *, #34866, .T. ) ;
#37387=EDGE_LOOP ( 'NONE', ( #8392, #5919 ) ) ;
#37393=( NAMED_UNIT ( * ) SI_UNIT ( $, .STERADIAN. ) SOLID_ANGLE_UNIT ( ) ) ;
#37437=AXIS2_PLACEMENT_3D ( 'NONE', #33506, #11689, #10986 ) ;
#37531=CARTESIAN_POINT ( 'NONE',  ( -0.1377952755905511861, -1.331775896911328393E-15, -0.7066929133858274037 ) ) ;
#37538=DIRECTION ( 'NONE',  ( 1.000000000000000000, 0.000000000000000000, 0.000000000000000000 ) ) ;
#37576=CARTESIAN_POINT ( 'NONE',  ( 0.6195511811023624027, 0.9842519685039365918, -0.7135826771653542844 ) ) ;
#37590=DIRECTION ( 'NONE',  ( -3.469446951953614189E-15, -1.000000000000000000, -1.118797478067273468E-31 ) ) ;
#37637=CONICAL_SURFACE ( 'NONE', #42199, 0.1003937007874010356, 0.7853981633978647237 ) ;
#37655=MECHANICAL_DESIGN_GEOMETRIC_PRESENTATION_REPRESENTATION('',(#25436),#45297);
#37680=ORIENTED_EDGE ( 'NONE', *, *, #4417, .F. ) ;
#37774=EDGE_CURVE ( 'NONE', #15018, #38595, #15681, .T. ) ;
#37817=VERTEX_POINT ( 'NONE', #11037 ) ;
#37847=VECTOR ( 'NONE', #17604, 39.37007874015748143 ) ;
#37911=AXIS2_PLACEMENT_3D ( 'NONE', #11411, #37040, #11657 ) ;
#37920=ORIENTED_EDGE ( 'NONE', *, *, #20125, .T. ) ;
#37964=CARTESIAN_POINT ( 'NONE',  ( 0.6195511811023595161, 0.1864803149606293620, -1.186023622047243986 ) ) ;
#38087=ORIENTED_EDGE ( 'NONE', *, *, #37325, .T. ) ;
#38113=EDGE_LOOP ( 'NONE', ( #31089, #32885 ) ) ;
#38116=CIRCLE ( 'NONE', #29744, 0.1968503937007874127 ) ;
#38183=LINE ( 'NONE', #41984, #21242 ) ;
#38251=DIRECTION ( 'NONE',  ( -0.000000000000000000, 1.000000000000000000, -3.995705278811693553E-31 ) ) ;
#38352=VECTOR ( 'NONE', #38993, 39.37007874015748143 ) ;
#38544=EDGE_CURVE ( 'NONE', #30859, #894, #41583, .T. ) ;
#38595=VERTEX_POINT ( 'NONE', #37297 ) ;
#38627=ADVANCED_FACE ( 'NONE', ( #22932 ), #15280, .F. ) ;
#38756=ORIENTED_EDGE ( 'NONE', *, *, #41511, .T. ) ;
#38885=EDGE_CURVE ( 'NONE', #30632, #5872, #46336, .T. ) ;
#38942=ADVANCED_FACE ( 'NONE', ( #3234 ), #10453, .F. ) ;
#38960=ORIENTED_EDGE ( 'NONE', *, *, #30443, .T. ) ;
#38970=EDGE_LOOP ( 'NONE', ( #8630, #23442, #32356, #14236 ) ) ;
#38993=DIRECTION ( 'NONE',  ( -3.469446951953613794E-15, -1.000000000000000000, 0.000000000000000000 ) ) ;
#39131=CARTESIAN_POINT ( 'NONE',  ( -0.4330708661417344563, 1.502516396515352363E-15, 4.927039740520691743E-17 ) ) ;
#39182=DIRECTION ( 'NONE',  ( 1.000000000000000000, -0.000000000000000000, -1.144917494144692682E-16 ) ) ;
#39186=CIRCLE ( 'NONE', #36173, 0.1013779527559055538 ) ;
#39210=ORIENTED_EDGE ( 'NONE', *, *, #46636, .T. ) ;
#39303=CARTESIAN_POINT ( 'NONE',  ( 0.6195511811023621807, 0.9842519685039365918, -1.186023622047243986 ) ) ;
#39395=CARTESIAN_POINT ( 'NONE',  ( 0.6195511811023612925, 0.6102362204724401940, 1.186023622047243986 ) ) ;
#39433=CIRCLE ( 'NONE', #40207, 0.1864803149606299171 ) ;
#39486=EDGE_LOOP ( 'NONE', ( #15081, #5620, #16649, #14760 ) ) ;
#39582=VERTEX_POINT ( 'NONE', #22314 ) ;
#39615=DIRECTION ( 'NONE',  ( 1.144917494144692682E-16, -5.091027988365947196E-31, 1.000000000000000000 ) ) ;
#39639=PLANE ( 'NONE',  #44162 ) ;
#39652=EDGE_LOOP ( 'NONE', ( #27644, #27868, #36434, #21762, #35651, #26032 ) ) ;
#39760=EDGE_LOOP ( 'NONE', ( #4394, #24964, #4642, #23244, #24057, #18367, #10235, #43739 ) ) ;
#39951=AXIS2_PLACEMENT_3D ( 'NONE', #12862, #27495, #42046 ) ;
#39989=LINE ( 'NONE', #17728, #27085 ) ;
#40009=DIRECTION ( 'NONE',  ( 1.000000000000000000, -3.469446951953614978E-15, -1.144917494144692929E-16 ) ) ;
#40083=CARTESIAN_POINT ( 'NONE',  ( 0.4330708661417291827, 1.006139616066731278E-16, 1.186023622047243986 ) ) ;
#40109=CARTESIAN_POINT ( 'NONE',  ( -0.2362204724409468770, 2.422684756221292845E-15, 1.186023622047244208 ) ) ;
#40116=CARTESIAN_POINT ( 'NONE',  ( 0.6195511811023624027, 0.9842519685039370358, -0.7135826771653542844 ) ) ;
#40177=CARTESIAN_POINT ( 'NONE',  ( 0.6195511811023612925, 0.6529540528279703659, 0.4629603087243970849 ) ) ;
#40207=AXIS2_PLACEMENT_3D ( 'NONE', #42909, #31934, #28338 ) ;
#40226=AXIS2_PLACEMENT_3D ( 'NONE', #6828, #39182, #47342 ) ;
#40238=EDGE_CURVE ( 'NONE', #15531, #40961, #25036, .T. ) ;
#40498=SHAPE_REPRESENTATION ( 'Side Bracket', ( #20860 ), #29349 ) ;
#40502=DIRECTION ( 'NONE',  ( -1.000000000000000000, 3.469446951953614189E-15, 1.144917494144692682E-16 ) ) ;
#40527=AXIS2_PLACEMENT_3D ( 'NONE', #5989, #31661, #32120 ) ;
#40578=FACE_OUTER_BOUND ( 'NONE', #13989, .T. ) ;
#40609=EDGE_CURVE ( 'NONE', #3381, #5872, #38183, .T. ) ;
#40614=AXIS2_PLACEMENT_3D ( 'NONE', #23939, #12697, #13165 ) ;
#40634=DIRECTION ( 'NONE',  ( 1.000000000000000000, -3.469446951953614583E-15, -1.144917494144684054E-16 ) ) ;
#40698=FACE_OUTER_BOUND ( 'NONE', #15876, .T. ) ;
#40712=VECTOR ( 'NONE', #25302, 39.37007874015748143 ) ;
#40771=DIRECTION ( 'NONE',  ( 1.000000000000000000, -3.469446951953614189E-15, 0.000000000000000000 ) ) ;
#40789=DIRECTION ( 'NONE',  ( 0.000000000000000000, 0.000000000000000000, 1.000000000000000000 ) ) ;
#40863=CARTESIAN_POINT ( 'NONE',  ( -0.1377952755905511861, 0.1564960629921283985, 0.9074803149606294195 ) ) ;
#40933=FACE_BOUND ( 'NONE', #37387, .T. ) ;
#40961=VERTEX_POINT ( 'NONE', #42932 ) ;
#40968=SHAPE_REPRESENTATION_RELATIONSHIP ( 'NONE' , 'NONE' ,  #40498, #43808 ) ;
#41049=VERTEX_POINT ( 'NONE', #6225 ) ;
#41111=LINE ( 'NONE', #37072, #11507 ) ;
#41116=ORIENTED_EDGE ( 'NONE', *, *, #14353, .T. ) ;
#41146=EDGE_LOOP ( 'NONE', ( #15726, #33781, #32595, #12942, #26544, #20829, #12996, #6733 ) ) ;
#41225=ORIENTED_EDGE ( 'NONE', *, *, #13961, .T. ) ;
#41230=CIRCLE ( 'NONE', #37437, 0.1624015748031507056 ) ;
#41289=DIRECTION ( 'NONE',  ( 8.659560562358538199E-17, 0.7071067811862530306, -0.7071067811868418929 ) ) ;
#41315=CARTESIAN_POINT ( 'NONE',  ( -0.2362204724409464329, 0.1574803149606323616, 1.186023622047244208 ) ) ;
#41355=CIRCLE ( 'NONE', #14611, 0.1624015748031505668 ) ;
#41356=LINE ( 'NONE', #34230, #10209 ) ;
#41364=AXIS2_PLACEMENT_3D ( 'NONE', #35937, #3097, #17723 ) ;
#41390=CARTESIAN_POINT ( 'NONE',  ( 0.6195511811023624027, 0.9842519685039365918, -0.7135826771653542844 ) ) ;
#41480=ORIENTED_EDGE ( 'NONE', *, *, #42061, .T. ) ;
#41495=CARTESIAN_POINT ( 'NONE',  ( 0.4620708661417356478, 0.9842519685039370358, -0.5511811023622036343 ) ) ;
#41511=EDGE_CURVE ( 'NONE', #7349, #45730, #43231, .T. ) ;
#41541=FACE_OUTER_BOUND ( 'NONE', #46907, .T. ) ;
#41574=CYLINDRICAL_SURFACE ( 'NONE', #12348, 0.1003937007874010356 ) ;
#41583=LINE ( 'NONE', #3997, #44813 ) ;
#41613=DIRECTION ( 'NONE',  ( -1.000000000000000000, 3.469446951953614189E-15, 1.144917494144692682E-16 ) ) ;
#41769=LINE ( 'NONE', #27218, #26622 ) ;
#41842=FACE_OUTER_BOUND ( 'NONE', #29936, .T. ) ;
#41850=ADVANCED_FACE ( 'NONE', ( #41842 ), #27049, .T. ) ;
#41872=PLANE ( 'NONE',  #26989 ) ;
#41957=LINE ( 'NONE', #12777, #12793 ) ;
#41984=CARTESIAN_POINT ( 'NONE',  ( -0.1377952755905511861, 0.1574803149606320007, -0.7066929133858274037 ) ) ;
#42017=ORIENTED_EDGE ( 'NONE', *, *, #24214, .T. ) ;
#42021=DIRECTION ( 'NONE',  ( 1.000000000000000000, -3.469446951953614583E-15, -1.144917494144684547E-16 ) ) ;
#42046=DIRECTION ( 'NONE',  ( -1.000000000000000000, 0.000000000000000000, 0.000000000000000000 ) ) ;
#42061=EDGE_CURVE ( 'NONE', #36671, #27780, #15736, .T. ) ;
#42131=AXIS2_PLACEMENT_3D ( 'NONE', #42308, #31792, #34673 ) ;
#42199=AXIS2_PLACEMENT_3D ( 'NONE', #14963, #22129, #21419 ) ;
#42216=FACE_OUTER_BOUND ( 'NONE', #9967, .T. ) ;
#42308=CARTESIAN_POINT ( 'NONE',  ( -0.2362204724409464052, 0.1574803149606323616, 0.9891732283464568232 ) ) ;
#42452=PRODUCT_CONTEXT ( 'NONE', #3691, 'mechanical' ) ;
#42479=VERTEX_POINT ( 'NONE', #3975 ) ;
#42496=DIRECTION ( 'NONE',  ( 0.000000000000000000, 1.000000000000000000, 0.000000000000000000 ) ) ;
#42497=AXIS2_PLACEMENT_3D ( 'NONE', #21960, #33478, #371 ) ;
#42645=PLANE ( 'NONE',  #10671 ) ;
#42858=AXIS2_PLACEMENT_3D ( 'NONE', #35618, #43734, #6832 ) ;
#42867=CARTESIAN_POINT ( 'NONE',  ( -0.1377952755905511861, 0.1564960629921283985, -0.7066929133858274037 ) ) ;
#42909=CARTESIAN_POINT ( 'NONE',  ( 0.4330708661417295158, 0.1864803149606300281, -1.186023622047243986 ) ) ;
#42932=CARTESIAN_POINT ( 'NONE',  ( -0.1377952755905511584, 0.1574803149606320007, 0.7057086614173230243 ) ) ;
#42976=EDGE_CURVE ( 'NONE', #6860, #2262, #39433, .T. ) ;
#42991=CARTESIAN_POINT ( 'NONE',  ( 0.4620708661417345375, 0.6102362204724407491, 0.9891732283464566011 ) ) ;
#43026=VECTOR ( 'NONE', #27956, 39.37007874015748143 ) ;
#43041=FACE_OUTER_BOUND ( 'NONE', #35382, .T. ) ;
#43054=DIRECTION ( 'NONE',  ( -3.469446951953614978E-15, -1.000000000000000000, 3.995705278811693553E-31 ) ) ;
#43111=CARTESIAN_POINT ( 'NONE',  ( 0.4330708661417327909, 0.1574803149606300301, -1.186023622047243986 ) ) ;
#43197=EDGE_LOOP ( 'NONE', ( #22492, #46502, #1302, #24596 ) ) ;
#43218=AXIS2_PLACEMENT_3D ( 'NONE', #2086, #31585, #27776 ) ;
#43231=LINE ( 'NONE', #39395, #37847 ) ;
#43253=DIRECTION ( 'NONE',  ( 0.000000000000000000, 1.000000000000000000, 0.000000000000000000 ) ) ;
#43611=LINE ( 'NONE', #10821, #35802 ) ;
#43641=CIRCLE ( 'NONE', #29175, 0.1864803149606299448 ) ;
#43687=LINE ( 'NONE', #40083, #16043 ) ;
#43734=DIRECTION ( 'NONE',  ( -1.000000000000000000, 3.469446951953614189E-15, 1.144917494144692682E-16 ) ) ;
#43739=ORIENTED_EDGE ( 'NONE', *, *, #42976, .T. ) ;
#43777=ORIENTED_EDGE ( 'NONE', *, *, #26865, .T. ) ;
#43808=ADVANCED_BREP_SHAPE_REPRESENTATION ( 'Side Bracket', ( #36893, #20860 ), #29349 ) ;
#43836=DIRECTION ( 'NONE',  ( 1.000000000000000000, -3.532562060772751952E-15, 0.000000000000000000 ) ) ;
#43955=DIRECTION ( 'NONE',  ( -1.000000000000000000, 3.469446951953613794E-15, 1.144917494144684547E-16 ) ) ;
#44072=CARTESIAN_POINT ( 'NONE',  ( -0.1377952755905511584, -1.331775896911328393E-15, 0.7066929133858274037 ) ) ;
#44113=CARTESIAN_POINT ( 'NONE',  ( -0.4330708661417337901, 0.1574803149606330277, 1.186023622047244208 ) ) ;
#44162=AXIS2_PLACEMENT_3D ( 'NONE', #33446, #561, #22385 ) ;
#44195=EDGE_CURVE ( 'NONE', #2533, #9932, #8874, .T. ) ;
#44287=DIRECTION ( 'NONE',  ( 1.000000000000000000, -3.368395098984090098E-15, 0.000000000000000000 ) ) ;
#44375=ORIENTED_EDGE ( 'NONE', *, *, #38885, .T. ) ;
#44386=FACE_OUTER_BOUND ( 'NONE', #30526, .T. ) ;
#44408=CARTESIAN_POINT ( 'NONE',  ( -0.4330708661417343452, 3.105646754637359143E-15, 0.9891732283464568232 ) ) ;
#44439=DIRECTION ( 'NONE',  ( -0.000000000000000000, 1.000000000000000000, -3.995705278811693553E-31 ) ) ;
#44466=DIRECTION ( 'NONE',  ( 3.469446951953614583E-15, 1.000000000000000000, 1.751623080406021339E-46 ) ) ;
#44471=EDGE_LOOP ( 'NONE', ( #22177, #16276, #15589, #44716, #37330, #2306, #33832, #7442 ) ) ;
#44496=DIRECTION ( 'NONE',  ( -1.000000000000000000, 3.469446951953613794E-15, 0.000000000000000000 ) ) ;
#44519=VECTOR ( 'NONE', #43955, 39.37007874015748143 ) ;
#44649=VECTOR ( 'NONE', #14843, 39.37007874015748143 ) ;
#44716=ORIENTED_EDGE ( 'NONE', *, *, #2315, .T. ) ;
#44813=VECTOR ( 'NONE', #40634, 39.37007874015748143 ) ;
#44857=ORIENTED_EDGE ( 'NONE', *, *, #13253, .F. ) ;
#44898=ADVANCED_FACE ( 'NONE', ( #25574 ), #11415, .F. ) ;
#44968=DIRECTION ( 'NONE',  ( -0.000000000000000000, 1.000000000000000000, -3.995705278811693553E-31 ) ) ;
#45158=CARTESIAN_POINT ( 'NONE',  ( 0.6195511811023612925, 0.6102362204724403050, 0.5854071585544579071 ) ) ;
#45220=CYLINDRICAL_SURFACE ( 'NONE', #46960, 0.4724409448818900348 ) ;
#45242=CARTESIAN_POINT ( 'NONE',  ( -0.1377952755905511861, -1.331775896911328393E-15, 0.9074803149606294195 ) ) ;
#45275=AXIS2_PLACEMENT_3D ( 'NONE', #3292, #18155, #6646 ) ;
#45286=DIRECTION ( 'NONE',  ( 0.000000000000000000, 0.000000000000000000, 1.000000000000000000 ) ) ;
#45297=( GEOMETRIC_REPRESENTATION_CONTEXT ( 3 ) GLOBAL_UNCERTAINTY_ASSIGNED_CONTEXT ( ( #33040 ) ) GLOBAL_UNIT_ASSIGNED_CONTEXT ( ( #21619, #22084, #25213 ) ) REPRESENTATION_CONTEXT ( 'NONE', 'WORKASPACE' ) ) ;
#45397=FACE_OUTER_BOUND ( 'NONE', #10211, .T. ) ;
#45530=CARTESIAN_POINT ( 'NONE',  ( 0.6195511811023590720, -5.463695987328343027E-16, 1.186023622047243986 ) ) ;
#45571=SHAPE_DEFINITION_REPRESENTATION ( #30345, #40498 ) ;
#45645=CYLINDRICAL_SURFACE ( 'NONE', #39951, 0.1864803149606299171 ) ;
#45646=DIRECTION ( 'NONE',  ( -1.000000000000000000, 3.469446951953614189E-15, 1.144917494144692682E-16 ) ) ;
#45730=VERTEX_POINT ( 'NONE', #45158 ) ;
#45916=ADVANCED_FACE ( 'NONE', ( #11362 ), #37637, .F. ) ;
#45918=ORIENTED_EDGE ( 'NONE', *, *, #786, .T. ) ;
#45931=CIRCLE ( 'NONE', #42858, 0.1624015748031505668 ) ;
#46016=ORIENTED_EDGE ( 'NONE', *, *, #18029, .F. ) ;
#46041=ORIENTED_EDGE ( 'NONE', *, *, #34067, .F. ) ;
#46055=COLOUR_RGB ( '', 0.09019608, 0.27058824, 0.51372549) ;
#46135=ADVANCED_FACE ( 'NONE', ( #30309 ), #23081, .F. ) ;
#46296=ADVANCED_FACE ( 'NONE', ( #44386 ), #17720, .F. ) ;
#46336=CIRCLE ( 'NONE', #30376, 0.1003937007874010356 ) ;
#46340=VERTEX_POINT ( 'NONE', #28334 ) ;
#46502=ORIENTED_EDGE ( 'NONE', *, *, #10903, .F. ) ;
#46513=CIRCLE ( 'NONE', #5195, 0.1013779527559055538 ) ;
#46523=DIRECTION ( 'NONE',  ( 1.000000000000000000, -0.000000000000000000, -1.144917494144692682E-16 ) ) ;
#46557=DIRECTION ( 'NONE',  ( 3.469446951953614583E-15, 1.000000000000000000, 0.000000000000000000 ) ) ;
#46573=CARTESIAN_POINT ( 'NONE',  ( -0.4330708661417343452, 3.105646754637359143E-15, 1.186023622047244430 ) ) ;
#46636=EDGE_CURVE ( 'NONE', #32133, #7349, #2891, .T. ) ;
#46853=VECTOR ( 'NONE', #8492, 39.37007874015748143 ) ;
#46907=EDGE_LOOP ( 'NONE', ( #2807, #47053, #6321, #26738 ) ) ;
#46958=PRESENTATION_STYLE_ASSIGNMENT (( #35487 ) ) ;
#46960=AXIS2_PLACEMENT_3D ( 'NONE', #37576, #41613, #8819 ) ;
#46969=ORIENTED_EDGE ( 'NONE', *, *, #24032, .T. ) ;
#46989=ADVANCED_FACE ( 'NONE', ( #43041 ), #23143, .F. ) ;
#47025=FACE_BOUND ( 'NONE', #15365, .T. ) ;
#47033=AXIS2_PLACEMENT_3D ( 'NONE', #549, #21917, #28903 ) ;
#47053=ORIENTED_EDGE ( 'NONE', *, *, #38544, .F. ) ;
#47100=LINE ( 'NONE', #14524, #25529 ) ;
#47153=LINE ( 'NONE', #14337, #31428 ) ;
#47342=DIRECTION ( 'NONE',  ( 0.000000000000000000, 0.000000000000000000, -1.000000000000000000 ) ) ;
#47431=CARTESIAN_POINT ( 'NONE',  ( 0.4620708661417324281, 7.036468458233680972E-30, 1.186023622047243986 ) ) ;
#47439=DIRECTION ( 'NONE',  ( 0.000000000000000000, 0.000000000000000000, -1.000000000000000000 ) ) ;
#47441=DIRECTION ( 'NONE',  ( 3.469446951953614978E-15, 1.000000000000000000, -3.995705278811693553E-31 ) ) ;
ENDSEC;
END-ISO-10303-21;
